ISO-10303-21;
HEADER;
/* Generated by software containing ST-Developer
 * from STEP Tools, Inc. (www.steptools.com) 
 */

FILE_DESCRIPTION(
/* description */ (''),
/* implementation_level */ '2;1');

FILE_NAME(
/* name */ '08_Mechanical_Seal_Seat.step',
/* time_stamp */ '2026-10-26T04:15:57-07:00',
/* author */ (''),
/* organization */ (''),
/* preprocessor_version */ 'ST-DEVELOPER v20.2',
/* originating_system */ 'Autodesk Translation Framework v15.15.0.0',
/* authorisation */ '');

FILE_SCHEMA (('AUTOMOTIVE_DESIGN { 1 0 10303 214 3 1 1 }'));
ENDSEC;

DATA;
#10=MECHANICAL_DESIGN_GEOMETRIC_PRESENTATION_REPRESENTATION('',(#459),#55737);
#376=CONICAL_SURFACE('',#29172,19.75,0.785398163397451);
#419=SHAPE_REPRESENTATION_RELATIONSHIP('SRR','None',#55828,#439);
#439=ADVANCED_BREP_SHAPE_REPRESENTATION('',(#479),#55724);
#459=STYLED_ITEM('',(#55998),#479);
#479=MANIFOLD_SOLID_BREP('Body1',#27228);
#700=FACE_BOUND('',#9508,.T.);
#701=FACE_BOUND('',#9512,.T.);
#1391=PLANE('',#29170);
#1392=PLANE('',#29176);
#3332=LINE('',#45228,#5703);
#3333=LINE('',#45236,#5704);
#3334=LINE('',#45240,#5705);
#5703=VECTOR('',#34964,13.);
#5704=VECTOR('',#34975,19.75);
#5705=VECTOR('',#34980,20.);
#6689=CYLINDRICAL_SURFACE('',#29167,13.);
#6690=CYLINDRICAL_SURFACE('',#29174,20.);
#7841=FACE_OUTER_BOUND('',#9506,.T.);
#7842=FACE_OUTER_BOUND('',#9507,.T.);
#7843=FACE_OUTER_BOUND('',#9509,.T.);
#7844=FACE_OUTER_BOUND('',#9510,.T.);
#7845=FACE_OUTER_BOUND('',#9511,.T.);
#9506=EDGE_LOOP('',(#22960,#22961,#22962,#22963));
#9507=EDGE_LOOP('',(#22964));
#9508=EDGE_LOOP('',(#22965));
#9509=EDGE_LOOP('',(#22966,#22967,#22968,#22969));
#9510=EDGE_LOOP('',(#22970,#22971,#22972,#22973));
#9511=EDGE_LOOP('',(#22974));
#9512=EDGE_LOOP('',(#22975));
#10767=CIRCLE('',#29168,13.);
#10768=CIRCLE('',#29169,13.);
#10769=CIRCLE('',#29171,19.5);
#10770=CIRCLE('',#29173,20.);
#10771=CIRCLE('',#29175,20.);
#13078=VERTEX_POINT('',#45225);
#13079=VERTEX_POINT('',#45227);
#13080=VERTEX_POINT('',#45231);
#13081=VERTEX_POINT('',#45234);
#13082=VERTEX_POINT('',#45238);
#16484=EDGE_CURVE('',#13078,#13078,#10767,.T.);
#16485=EDGE_CURVE('',#13078,#13079,#3332,.T.);
#16486=EDGE_CURVE('',#13079,#13079,#10768,.T.);
#16487=EDGE_CURVE('',#13080,#13080,#10769,.T.);
#16488=EDGE_CURVE('',#13081,#13081,#10770,.T.);
#16489=EDGE_CURVE('',#13081,#13080,#3333,.T.);
#16490=EDGE_CURVE('',#13082,#13082,#10771,.T.);
#16491=EDGE_CURVE('',#13082,#13081,#3334,.T.);
#22960=ORIENTED_EDGE('',*,*,#16484,.T.);
#22961=ORIENTED_EDGE('',*,*,#16485,.T.);
#22962=ORIENTED_EDGE('',*,*,#16486,.F.);
#22963=ORIENTED_EDGE('',*,*,#16485,.F.);
#22964=ORIENTED_EDGE('',*,*,#16487,.F.);
#22965=ORIENTED_EDGE('',*,*,#16486,.T.);
#22966=ORIENTED_EDGE('',*,*,#16488,.F.);
#22967=ORIENTED_EDGE('',*,*,#16489,.T.);
#22968=ORIENTED_EDGE('',*,*,#16487,.T.);
#22969=ORIENTED_EDGE('',*,*,#16489,.F.);
#22970=ORIENTED_EDGE('',*,*,#16490,.F.);
#22971=ORIENTED_EDGE('',*,*,#16491,.T.);
#22972=ORIENTED_EDGE('',*,*,#16488,.T.);
#22973=ORIENTED_EDGE('',*,*,#16491,.F.);
#22974=ORIENTED_EDGE('',*,*,#16490,.T.);
#22975=ORIENTED_EDGE('',*,*,#16484,.F.);
#26665=ADVANCED_FACE('',(#7841),#6689,.F.);
#26666=ADVANCED_FACE('',(#7842,#700),#1391,.T.);
#26667=ADVANCED_FACE('',(#7843),#376,.T.);
#26668=ADVANCED_FACE('',(#7844),#6690,.T.);
#26669=ADVANCED_FACE('',(#7845,#701),#1392,.T.);
#27228=CLOSED_SHELL('',(#26665,#26666,#26667,#26668,#26669));
#29166=AXIS2_PLACEMENT_3D('',#45223,#34958,#34959);
#29167=AXIS2_PLACEMENT_3D('',#45224,#34960,#34961);
#29168=AXIS2_PLACEMENT_3D('',#45226,#34962,#34963);
#29169=AXIS2_PLACEMENT_3D('',#45229,#34965,#34966);
#29170=AXIS2_PLACEMENT_3D('',#45230,#34967,#34968);
#29171=AXIS2_PLACEMENT_3D('',#45232,#34969,#34970);
#29172=AXIS2_PLACEMENT_3D('',#45233,#34971,#34972);
#29173=AXIS2_PLACEMENT_3D('',#45235,#34973,#34974);
#29174=AXIS2_PLACEMENT_3D('',#45237,#34976,#34977);
#29175=AXIS2_PLACEMENT_3D('',#45239,#34978,#34979);
#29176=AXIS2_PLACEMENT_3D('',#45241,#34981,#34982);
#34958=DIRECTION('axis',(0.,0.,1.));
#34959=DIRECTION('refdir',(1.,0.,0.));
#34960=DIRECTION('center_axis',(1.,0.,0.));
#34961=DIRECTION('ref_axis',(0.,1.,0.));
#34962=DIRECTION('center_axis',(1.,0.,0.));
#34963=DIRECTION('ref_axis',(0.,0.,-1.));
#34964=DIRECTION('',(-1.,0.,0.));
#34965=DIRECTION('center_axis',(1.,0.,0.));
#34966=DIRECTION('ref_axis',(0.,0.,-1.));
#34967=DIRECTION('center_axis',(-1.,0.,0.));
#34968=DIRECTION('ref_axis',(0.,0.,1.));
#34969=DIRECTION('center_axis',(1.,0.,0.));
#34970=DIRECTION('ref_axis',(0.,0.,-1.));
#34971=DIRECTION('center_axis',(1.,0.,0.));
#34972=DIRECTION('ref_axis',(0.,1.,0.));
#34973=DIRECTION('center_axis',(1.,0.,0.));
#34974=DIRECTION('ref_axis',(0.,0.,-1.));
#34975=DIRECTION('',(-0.707106781186546,0.707106781186549,8.65956056235495E-17));
#34976=DIRECTION('center_axis',(1.,0.,0.));
#34977=DIRECTION('ref_axis',(0.,1.,0.));
#34978=DIRECTION('center_axis',(1.,0.,0.));
#34979=DIRECTION('ref_axis',(0.,0.,-1.));
#34980=DIRECTION('',(-1.,0.,0.));
#34981=DIRECTION('center_axis',(1.,0.,0.));
#34982=DIRECTION('ref_axis',(0.,0.,-1.));
#45223=CARTESIAN_POINT('',(0.,0.,0.));
#45224=CARTESIAN_POINT('Origin',(26.,0.,0.));
#45225=CARTESIAN_POINT('',(30.,-13.,-1.59204083889156E-15));
#45226=CARTESIAN_POINT('Origin',(30.,0.,0.));
#45227=CARTESIAN_POINT('',(22.,-13.,-1.59204083889156E-15));
#45228=CARTESIAN_POINT('',(26.,-13.,-1.59204083889156E-15));
#45229=CARTESIAN_POINT('Origin',(22.,0.,0.));
#45230=CARTESIAN_POINT('Origin',(22.,19.5,0.));
#45231=CARTESIAN_POINT('',(22.,-19.5,-2.38806125833734E-15));
#45232=CARTESIAN_POINT('Origin',(22.,0.,0.));
#45233=CARTESIAN_POINT('Origin',(22.25,0.,0.));
#45234=CARTESIAN_POINT('',(22.5,-20.,-2.44929359829471E-15));
#45235=CARTESIAN_POINT('Origin',(22.5,0.,0.));
#45236=CARTESIAN_POINT('',(22.25,-19.75,-2.41867742831602E-15));
#45237=CARTESIAN_POINT('Origin',(26.25,0.,0.));
#45238=CARTESIAN_POINT('',(30.,-20.,-2.44929359829471E-15));
#45239=CARTESIAN_POINT('Origin',(30.,0.,0.));
#45240=CARTESIAN_POINT('',(26.25,-20.,-2.44929359829471E-15));
#45241=CARTESIAN_POINT('Origin',(30.,13.,0.));
#55702=UNCERTAINTY_MEASURE_WITH_UNIT(LENGTH_MEASURE(0.01),#55738,
'DISTANCE_ACCURACY_VALUE',
'Maximum model space distance between geometric entities at asserted c
onnectivities');
#55715=UNCERTAINTY_MEASURE_WITH_UNIT(LENGTH_MEASURE(0.01),#55738,
'DISTANCE_ACCURACY_VALUE',
'Maximum model space distance between geometric entities at asserted c
onnectivities');
#55724=(
GEOMETRIC_REPRESENTATION_CONTEXT(3)
GLOBAL_UNCERTAINTY_ASSIGNED_CONTEXT((#55702))
GLOBAL_UNIT_ASSIGNED_CONTEXT((#55738,#55740,#55741))
REPRESENTATION_CONTEXT('','3D')
);
#55737=(
GEOMETRIC_REPRESENTATION_CONTEXT(3)
GLOBAL_UNCERTAINTY_ASSIGNED_CONTEXT((#55715))
GLOBAL_UNIT_ASSIGNED_CONTEXT((#55738,#55740,#55741))
REPRESENTATION_CONTEXT('','3D')
);
#55738=(
LENGTH_UNIT()
NAMED_UNIT(*)
SI_UNIT(.MILLI.,.METRE.)
);
#55740=(
NAMED_UNIT(*)
PLANE_ANGLE_UNIT()
SI_UNIT($,.RADIAN.)
);
#55741=(
NAMED_UNIT(*)
SI_UNIT($,.STERADIAN.)
SOLID_ANGLE_UNIT()
);
#55750=SHAPE_DEFINITION_REPRESENTATION(#55771,#55828);
#55771=PRODUCT_DEFINITION_SHAPE('',$,#55850);
#55828=SHAPE_REPRESENTATION('',(#29166),#55724);
#55841=PRODUCT_DEFINITION_CONTEXT('part definition',#55906,'design');
#55850=PRODUCT_DEFINITION('2026-10-26-00-34-24-473',
'08_Mechanical_Seal_Seat',#55871,#55841);
#55871=PRODUCT_DEFINITION_FORMATION('',$,#55916);
#55906=APPLICATION_CONTEXT(
'Core Data for Automotive Mechanical Design Process');
#55907=PRODUCT_CONTEXT('part definition',#55906,'mechanical');
#55916=PRODUCT('2026-10-26-00-34-24-473','08_Mechanical_Seal_Seat',$,(#55907));
#55992=COLOUR_RGB('Black',0.12,0.14,0.17);
#55993=FILL_AREA_STYLE_COLOUR('',#55992);
#55994=FILL_AREA_STYLE('',(#55993));
#55995=SURFACE_STYLE_FILL_AREA(#55994);
#55996=SURFACE_SIDE_STYLE('',(#55995));
#55997=SURFACE_STYLE_USAGE(.BOTH.,#55996);
#55998=PRESENTATION_STYLE_ASSIGNMENT((#55997));
ENDSEC;
END-ISO-10303-21;
